ISO-10303-21;
HEADER;
/* Generated by software containing ST-Developer
 * from STEP Tools, Inc. (www.steptools.com) 
 */

FILE_DESCRIPTION(
/* description */ (''),
/* implementation_level */ '2;1');

FILE_NAME(
/* name */ 'M3_Nut_01 (1).step',
/* time_stamp */ '2026-10-22T15:07:41+06:00',
/* author */ (''),
/* organization */ (''),
/* preprocessor_version */ 'ST-DEVELOPER v20.2',
/* originating_system */ 'Autodesk Translation Framework v15.15.0.0',
/* authorisation */ '');

FILE_SCHEMA (('AUTOMOTIVE_DESIGN { 1 0 10303 214 3 1 1 }'));
ENDSEC;

DATA;
#10=MECHANICAL_DESIGN_GEOMETRIC_PRESENTATION_REPRESENTATION('',(#2885),#19220);
#74=SHAPE_REPRESENTATION_RELATIONSHIP('SRR','None',#19277,#88);
#88=ADVANCED_BREP_SHAPE_REPRESENTATION('',(#102),#19213);
#102=MANIFOLD_SOLID_BREP('M3_Nut_01',#11321);
#565=FACE_BOUND('',#4313,.T.);
#566=FACE_BOUND('',#4315,.T.);
#752=PLANE('',#12480);
#753=PLANE('',#12481);
#754=PLANE('',#12482);
#755=PLANE('',#12483);
#756=PLANE('',#12484);
#757=PLANE('',#12485);
#758=PLANE('',#12486);
#759=PLANE('',#12487);
#1430=LINE('',#18438,#2285);
#1431=LINE('',#18443,#2286);
#1432=LINE('',#18445,#2287);
#1433=LINE('',#18447,#2288);
#1434=LINE('',#18448,#2289);
#1435=LINE('',#18451,#2290);
#1436=LINE('',#18453,#2291);
#1437=LINE('',#18454,#2292);
#1438=LINE('',#18457,#2293);
#1439=LINE('',#18459,#2294);
#1440=LINE('',#18460,#2295);
#1441=LINE('',#18463,#2296);
#1442=LINE('',#18465,#2297);
#1443=LINE('',#18466,#2298);
#1444=LINE('',#18469,#2299);
#1445=LINE('',#18471,#2300);
#1446=LINE('',#18472,#2301);
#1447=LINE('',#18474,#2302);
#1448=LINE('',#18475,#2303);
#2285=VECTOR('',#15311,1.49999999999999);
#2286=VECTOR('',#15316,10.);
#2287=VECTOR('',#15317,10.);
#2288=VECTOR('',#15318,10.);
#2289=VECTOR('',#15319,10.);
#2290=VECTOR('',#15322,10.);
#2291=VECTOR('',#15323,10.);
#2292=VECTOR('',#15324,10.);
#2293=VECTOR('',#15327,10.);
#2294=VECTOR('',#15328,10.);
#2295=VECTOR('',#15329,10.);
#2296=VECTOR('',#15332,10.);
#2297=VECTOR('',#15333,10.);
#2298=VECTOR('',#15334,10.);
#2299=VECTOR('',#15337,10.);
#2300=VECTOR('',#15338,10.);
#2301=VECTOR('',#15339,10.);
#2302=VECTOR('',#15342,10.);
#2303=VECTOR('',#15343,10.);
#2828=CYLINDRICAL_SURFACE('',#12477,1.465);
#2885=STYLED_ITEM('',(#19410),#102);
#3303=FACE_OUTER_BOUND('',#4305,.T.);
#3304=FACE_OUTER_BOUND('',#4306,.T.);
#3305=FACE_OUTER_BOUND('',#4307,.T.);
#3306=FACE_OUTER_BOUND('',#4308,.T.);
#3307=FACE_OUTER_BOUND('',#4309,.T.);
#3308=FACE_OUTER_BOUND('',#4310,.T.);
#3309=FACE_OUTER_BOUND('',#4311,.T.);
#3310=FACE_OUTER_BOUND('',#4312,.T.);
#3311=FACE_OUTER_BOUND('',#4314,.T.);
#4305=EDGE_LOOP('',(#10042,#10043,#10044,#10045));
#4306=EDGE_LOOP('',(#10046,#10047,#10048,#10049));
#4307=EDGE_LOOP('',(#10050,#10051,#10052,#10053));
#4308=EDGE_LOOP('',(#10054,#10055,#10056,#10057));
#4309=EDGE_LOOP('',(#10058,#10059,#10060,#10061));
#4310=EDGE_LOOP('',(#10062,#10063,#10064,#10065));
#4311=EDGE_LOOP('',(#10066,#10067,#10068,#10069));
#4312=EDGE_LOOP('',(#10070,#10071,#10072,#10073,#10074,#10075));
#4313=EDGE_LOOP('',(#10076));
#4314=EDGE_LOOP('',(#10077,#10078,#10079,#10080,#10081,#10082));
#4315=EDGE_LOOP('',(#10083));
#5075=CIRCLE('',#12478,1.465);
#5076=CIRCLE('',#12479,1.465);
#5947=VERTEX_POINT('',#18435);
#5948=VERTEX_POINT('',#18437);
#5949=VERTEX_POINT('',#18441);
#5950=VERTEX_POINT('',#18442);
#5951=VERTEX_POINT('',#18444);
#5952=VERTEX_POINT('',#18446);
#5953=VERTEX_POINT('',#18450);
#5954=VERTEX_POINT('',#18452);
#5955=VERTEX_POINT('',#18456);
#5956=VERTEX_POINT('',#18458);
#5957=VERTEX_POINT('',#18462);
#5958=VERTEX_POINT('',#18464);
#5959=VERTEX_POINT('',#18468);
#5960=VERTEX_POINT('',#18470);
#7352=EDGE_CURVE('',#5947,#5947,#5075,.T.);
#7353=EDGE_CURVE('',#5947,#5948,#1430,.T.);
#7354=EDGE_CURVE('',#5948,#5948,#5076,.F.);
#7355=EDGE_CURVE('',#5949,#5950,#1431,.T.);
#7356=EDGE_CURVE('',#5949,#5951,#1432,.T.);
#7357=EDGE_CURVE('',#5952,#5951,#1433,.T.);
#7358=EDGE_CURVE('',#5950,#5952,#1434,.T.);
#7359=EDGE_CURVE('',#5950,#5953,#1435,.T.);
#7360=EDGE_CURVE('',#5954,#5952,#1436,.T.);
#7361=EDGE_CURVE('',#5953,#5954,#1437,.T.);
#7362=EDGE_CURVE('',#5953,#5955,#1438,.T.);
#7363=EDGE_CURVE('',#5956,#5954,#1439,.T.);
#7364=EDGE_CURVE('',#5955,#5956,#1440,.T.);
#7365=EDGE_CURVE('',#5955,#5957,#1441,.T.);
#7366=EDGE_CURVE('',#5958,#5956,#1442,.T.);
#7367=EDGE_CURVE('',#5957,#5958,#1443,.T.);
#7368=EDGE_CURVE('',#5957,#5959,#1444,.T.);
#7369=EDGE_CURVE('',#5960,#5958,#1445,.T.);
#7370=EDGE_CURVE('',#5959,#5960,#1446,.T.);
#7371=EDGE_CURVE('',#5959,#5949,#1447,.T.);
#7372=EDGE_CURVE('',#5951,#5960,#1448,.T.);
#10042=ORIENTED_EDGE('',*,*,#7352,.F.);
#10043=ORIENTED_EDGE('',*,*,#7353,.T.);
#10044=ORIENTED_EDGE('',*,*,#7354,.F.);
#10045=ORIENTED_EDGE('',*,*,#7353,.F.);
#10046=ORIENTED_EDGE('',*,*,#7355,.F.);
#10047=ORIENTED_EDGE('',*,*,#7356,.T.);
#10048=ORIENTED_EDGE('',*,*,#7357,.F.);
#10049=ORIENTED_EDGE('',*,*,#7358,.F.);
#10050=ORIENTED_EDGE('',*,*,#7359,.F.);
#10051=ORIENTED_EDGE('',*,*,#7358,.T.);
#10052=ORIENTED_EDGE('',*,*,#7360,.F.);
#10053=ORIENTED_EDGE('',*,*,#7361,.F.);
#10054=ORIENTED_EDGE('',*,*,#7362,.F.);
#10055=ORIENTED_EDGE('',*,*,#7361,.T.);
#10056=ORIENTED_EDGE('',*,*,#7363,.F.);
#10057=ORIENTED_EDGE('',*,*,#7364,.F.);
#10058=ORIENTED_EDGE('',*,*,#7365,.F.);
#10059=ORIENTED_EDGE('',*,*,#7364,.T.);
#10060=ORIENTED_EDGE('',*,*,#7366,.F.);
#10061=ORIENTED_EDGE('',*,*,#7367,.F.);
#10062=ORIENTED_EDGE('',*,*,#7368,.F.);
#10063=ORIENTED_EDGE('',*,*,#7367,.T.);
#10064=ORIENTED_EDGE('',*,*,#7369,.F.);
#10065=ORIENTED_EDGE('',*,*,#7370,.F.);
#10066=ORIENTED_EDGE('',*,*,#7371,.F.);
#10067=ORIENTED_EDGE('',*,*,#7370,.T.);
#10068=ORIENTED_EDGE('',*,*,#7372,.F.);
#10069=ORIENTED_EDGE('',*,*,#7356,.F.);
#10070=ORIENTED_EDGE('',*,*,#7371,.T.);
#10071=ORIENTED_EDGE('',*,*,#7355,.T.);
#10072=ORIENTED_EDGE('',*,*,#7359,.T.);
#10073=ORIENTED_EDGE('',*,*,#7362,.T.);
#10074=ORIENTED_EDGE('',*,*,#7365,.T.);
#10075=ORIENTED_EDGE('',*,*,#7368,.T.);
#10076=ORIENTED_EDGE('',*,*,#7354,.T.);
#10077=ORIENTED_EDGE('',*,*,#7372,.T.);
#10078=ORIENTED_EDGE('',*,*,#7369,.T.);
#10079=ORIENTED_EDGE('',*,*,#7366,.T.);
#10080=ORIENTED_EDGE('',*,*,#7363,.T.);
#10081=ORIENTED_EDGE('',*,*,#7360,.T.);
#10082=ORIENTED_EDGE('',*,*,#7357,.T.);
#10083=ORIENTED_EDGE('',*,*,#7352,.T.);
#11179=ADVANCED_FACE('',(#3303),#2828,.F.);
#11180=ADVANCED_FACE('',(#3304),#752,.T.);
#11181=ADVANCED_FACE('',(#3305),#753,.T.);
#11182=ADVANCED_FACE('',(#3306),#754,.T.);
#11183=ADVANCED_FACE('',(#3307),#755,.T.);
#11184=ADVANCED_FACE('',(#3308),#756,.T.);
#11185=ADVANCED_FACE('',(#3309),#757,.T.);
#11186=ADVANCED_FACE('',(#3310,#565),#758,.T.);
#11187=ADVANCED_FACE('',(#3311,#566),#759,.F.);
#11321=CLOSED_SHELL('',(#11179,#11180,#11181,#11182,#11183,#11184,#11185,
#11186,#11187));
#12476=AXIS2_PLACEMENT_3D('',#18433,#15305,#15306);
#12477=AXIS2_PLACEMENT_3D('',#18434,#15307,#15308);
#12478=AXIS2_PLACEMENT_3D('',#18436,#15309,#15310);
#12479=AXIS2_PLACEMENT_3D('',#18439,#15312,#15313);
#12480=AXIS2_PLACEMENT_3D('',#18440,#15314,#15315);
#12481=AXIS2_PLACEMENT_3D('',#18449,#15320,#15321);
#12482=AXIS2_PLACEMENT_3D('',#18455,#15325,#15326);
#12483=AXIS2_PLACEMENT_3D('',#18461,#15330,#15331);
#12484=AXIS2_PLACEMENT_3D('',#18467,#15335,#15336);
#12485=AXIS2_PLACEMENT_3D('',#18473,#15340,#15341);
#12486=AXIS2_PLACEMENT_3D('',#18476,#15344,#15345);
#12487=AXIS2_PLACEMENT_3D('',#18477,#15346,#15347);
#15305=DIRECTION('axis',(0.,0.,1.));
#15306=DIRECTION('refdir',(1.,0.,0.));
#15307=DIRECTION('center_axis',(0.,-1.,0.));
#15308=DIRECTION('ref_axis',(-1.,0.,0.));
#15309=DIRECTION('center_axis',(0.,1.,0.));
#15310=DIRECTION('ref_axis',(-1.,0.,0.));
#15311=DIRECTION('',(0.,1.,0.));
#15312=DIRECTION('center_axis',(0.,1.,0.));
#15313=DIRECTION('ref_axis',(-1.,0.,0.));
#15314=DIRECTION('center_axis',(-0.866025403784439,0.,-0.499999999999999));
#15315=DIRECTION('ref_axis',(0.499999999999999,0.,-0.866025403784439));
#15316=DIRECTION('',(-0.499999999999999,0.,0.866025403784439));
#15317=DIRECTION('',(0.,-1.,0.));
#15318=DIRECTION('',(0.499999999999999,0.,-0.866025403784439));
#15319=DIRECTION('',(0.,-1.,0.));
#15320=DIRECTION('center_axis',(-0.866025403784439,0.,0.499999999999999));
#15321=DIRECTION('ref_axis',(-0.499999999999999,0.,-0.866025403784439));
#15322=DIRECTION('',(0.499999999999999,0.,0.866025403784439));
#15323=DIRECTION('',(-0.499999999999999,0.,-0.866025403784439));
#15324=DIRECTION('',(0.,-1.,0.));
#15325=DIRECTION('center_axis',(0.,0.,1.));
#15326=DIRECTION('ref_axis',(-1.,0.,0.));
#15327=DIRECTION('',(1.,0.,0.));
#15328=DIRECTION('',(-1.,0.,0.));
#15329=DIRECTION('',(0.,-1.,0.));
#15330=DIRECTION('center_axis',(0.866025403784438,0.,0.500000000000001));
#15331=DIRECTION('ref_axis',(-0.500000000000001,0.,0.866025403784438));
#15332=DIRECTION('',(0.500000000000001,0.,-0.866025403784438));
#15333=DIRECTION('',(-0.500000000000001,0.,0.866025403784438));
#15334=DIRECTION('',(0.,-1.,0.));
#15335=DIRECTION('center_axis',(0.866025403784439,0.,-0.5));
#15336=DIRECTION('ref_axis',(0.5,0.,0.866025403784439));
#15337=DIRECTION('',(-0.5,0.,-0.866025403784439));
#15338=DIRECTION('',(0.5,0.,0.866025403784439));
#15339=DIRECTION('',(0.,-1.,0.));
#15340=DIRECTION('center_axis',(4.61511044732058E-15,0.,-1.));
#15341=DIRECTION('ref_axis',(1.,0.,4.61511044732058E-15));
#15342=DIRECTION('',(-1.,0.,-4.61511044732058E-15));
#15343=DIRECTION('',(1.,0.,4.61511044732058E-15));
#15344=DIRECTION('center_axis',(0.,1.,0.));
#15345=DIRECTION('ref_axis',(-1.,0.,0.));
#15346=DIRECTION('center_axis',(0.,1.,0.));
#15347=DIRECTION('ref_axis',(-1.,0.,0.));
#18433=CARTESIAN_POINT('',(0.,0.,0.));
#18434=CARTESIAN_POINT('Origin',(363.987734179926,62.5,25.7372649179816));
#18435=CARTESIAN_POINT('',(365.452734179926,60.5,25.7372649179816));
#18436=CARTESIAN_POINT('Origin',(363.987734179926,60.5,25.7372649179816));
#18437=CARTESIAN_POINT('',(365.452734179926,62.5,25.7372649179816));
#18438=CARTESIAN_POINT('',(365.452734179926,62.5,25.7372649179816));
#18439=CARTESIAN_POINT('Origin',(363.987734179926,62.5,25.7372649179816));
#18440=CARTESIAN_POINT('Origin',(361.100982833978,62.5,25.7372649179816));
#18441=CARTESIAN_POINT('',(362.544358506952,62.5,23.2372649179816));
#18442=CARTESIAN_POINT('',(361.100982833978,62.5,25.7372649179816));
#18443=CARTESIAN_POINT('',(362.544358506952,62.5,23.2372649179816));
#18444=CARTESIAN_POINT('',(362.544358506952,60.5,23.2372649179816));
#18445=CARTESIAN_POINT('',(362.544358506952,62.5,23.2372649179816));
#18446=CARTESIAN_POINT('',(361.100982833978,60.5,25.7372649179816));
#18447=CARTESIAN_POINT('',(362.544358506952,60.5,23.2372649179816));
#18448=CARTESIAN_POINT('',(361.100982833978,62.5,25.7372649179816));
#18449=CARTESIAN_POINT('Origin',(362.544358506952,62.5,28.2372649179815));
#18450=CARTESIAN_POINT('',(362.544358506952,62.5,28.2372649179815));
#18451=CARTESIAN_POINT('',(361.100982833978,62.5,25.7372649179816));
#18452=CARTESIAN_POINT('',(362.544358506952,60.5,28.2372649179815));
#18453=CARTESIAN_POINT('',(361.100982833978,60.5,25.7372649179816));
#18454=CARTESIAN_POINT('',(362.544358506952,62.5,28.2372649179815));
#18455=CARTESIAN_POINT('Origin',(365.4311098529,62.5,28.2372649179815));
#18456=CARTESIAN_POINT('',(365.4311098529,62.5,28.2372649179815));
#18457=CARTESIAN_POINT('',(362.544358506952,62.5,28.2372649179815));
#18458=CARTESIAN_POINT('',(365.4311098529,60.5,28.2372649179815));
#18459=CARTESIAN_POINT('',(362.544358506952,60.5,28.2372649179815));
#18460=CARTESIAN_POINT('',(365.4311098529,62.5,28.2372649179815));
#18461=CARTESIAN_POINT('Origin',(366.874485525875,62.5,25.7372649179816));
#18462=CARTESIAN_POINT('',(366.874485525875,62.5,25.7372649179816));
#18463=CARTESIAN_POINT('',(365.4311098529,62.5,28.2372649179815));
#18464=CARTESIAN_POINT('',(366.874485525875,60.5,25.7372649179816));
#18465=CARTESIAN_POINT('',(365.4311098529,60.5,28.2372649179815));
#18466=CARTESIAN_POINT('',(366.874485525875,62.5,25.7372649179816));
#18467=CARTESIAN_POINT('Origin',(365.4311098529,62.5,23.2372649179816));
#18468=CARTESIAN_POINT('',(365.4311098529,62.5,23.2372649179816));
#18469=CARTESIAN_POINT('',(366.874485525875,62.5,25.7372649179816));
#18470=CARTESIAN_POINT('',(365.4311098529,60.5,23.2372649179816));
#18471=CARTESIAN_POINT('',(366.874485525875,60.5,25.7372649179816));
#18472=CARTESIAN_POINT('',(365.4311098529,62.5,23.2372649179816));
#18473=CARTESIAN_POINT('Origin',(362.544358506952,62.5,23.2372649179816));
#18474=CARTESIAN_POINT('',(365.4311098529,62.5,23.2372649179816));
#18475=CARTESIAN_POINT('',(365.4311098529,60.5,23.2372649179816));
#18476=CARTESIAN_POINT('Origin',(363.987734179926,62.5,25.7372649179816));
#18477=CARTESIAN_POINT('Origin',(363.987734179926,60.5,25.7372649179816));
#19197=UNCERTAINTY_MEASURE_WITH_UNIT(LENGTH_MEASURE(0.01),#19221,
'DISTANCE_ACCURACY_VALUE',
'Maximum model space distance between geometric entities at asserted c
onnectivities');
#19204=UNCERTAINTY_MEASURE_WITH_UNIT(LENGTH_MEASURE(0.01),#19221,
'DISTANCE_ACCURACY_VALUE',
'Maximum model space distance between geometric entities at asserted c
onnectivities');
#19213=(
GEOMETRIC_REPRESENTATION_CONTEXT(3)
GLOBAL_UNCERTAINTY_ASSIGNED_CONTEXT((#19197))
GLOBAL_UNIT_ASSIGNED_CONTEXT((#19221,#19223,#19224))
REPRESENTATION_CONTEXT('','3D')
);
#19220=(
GEOMETRIC_REPRESENTATION_CONTEXT(3)
GLOBAL_UNCERTAINTY_ASSIGNED_CONTEXT((#19204))
GLOBAL_UNIT_ASSIGNED_CONTEXT((#19221,#19223,#19224))
REPRESENTATION_CONTEXT('','3D')
);
#19221=(
LENGTH_UNIT()
NAMED_UNIT(*)
SI_UNIT(.MILLI.,.METRE.)
);
#19223=(
NAMED_UNIT(*)
PLANE_ANGLE_UNIT()
SI_UNIT($,.RADIAN.)
);
#19224=(
NAMED_UNIT(*)
SI_UNIT($,.STERADIAN.)
SOLID_ANGLE_UNIT()
);
#19233=SHAPE_DEFINITION_REPRESENTATION(#19248,#19277);
#19248=PRODUCT_DEFINITION_SHAPE('',$,#19293);
#19277=SHAPE_REPRESENTATION('',(#12476),#19213);
#19284=PRODUCT_DEFINITION_CONTEXT('part definition',#19331,'design');
#19293=PRODUCT_DEFINITION('M3_Nut_01 (1)','M3_Nut_01 (1)',#19308,#19284);
#19308=PRODUCT_DEFINITION_FORMATION('',$,#19341);
#19331=APPLICATION_CONTEXT(
'Core Data for Automotive Mechanical Design Process');
#19332=PRODUCT_CONTEXT('part definition',#19331,'mechanical');
#19341=PRODUCT('M3_Nut_01 (1)','M3_Nut_01 (1)',$,(#19332));
#19404=COLOUR_RGB('Black',0.12,0.14,0.17);
#19405=FILL_AREA_STYLE_COLOUR('',#19404);
#19406=FILL_AREA_STYLE('',(#19405));
#19407=SURFACE_STYLE_FILL_AREA(#19406);
#19408=SURFACE_SIDE_STYLE('',(#19407));
#19409=SURFACE_STYLE_USAGE(.BOTH.,#19408);
#19410=PRESENTATION_STYLE_ASSIGNMENT((#19409));
ENDSEC;
END-ISO-10303-21;
